ISO-10303-21;
HEADER;
/* Generated by software containing ST-Developer
 * from STEP Tools, Inc. (www.steptools.com) 
 */

FILE_DESCRIPTION(
/* description */ ('Air blow-off nozzle station'),
/* implementation_level */ '2;1');

FILE_NAME(
/* name */ 'Ball clamp nut (1).step',
/* time_stamp */ '2026-10-27T10:53:54-07:00',
/* author */ (''),
/* organization */ (''),
/* preprocessor_version */ 'ST-DEVELOPER v20.2',
/* originating_system */ 'Autodesk Translation Framework v15.17.0.0',
/* authorisation */ '');

FILE_SCHEMA (('AUTOMOTIVE_DESIGN { 1 0 10303 214 3 1 1 }'));
ENDSEC;

DATA;
#10=MECHANICAL_DESIGN_GEOMETRIC_PRESENTATION_REPRESENTATION('',(#244),#7897);
#166=SPHERICAL_SURFACE('',#4720,1.);
#194=SHAPE_REPRESENTATION_RELATIONSHIP('SRR','None',#8008,#219);
#219=ADVANCED_BREP_SHAPE_REPRESENTATION('',(#269),#7875);
#244=STYLED_ITEM('',(#8227),#269);
#269=MANIFOLD_SOLID_BREP('Body1',#4293);
#315=FACE_BOUND('',#898,.T.);
#316=FACE_BOUND('',#899,.T.);
#317=FACE_BOUND('',#902,.T.);
#318=FACE_BOUND('',#905,.T.);
#319=FACE_BOUND('',#907,.T.);
#418=PLANE('',#4725);
#419=PLANE('',#4729);
#420=PLANE('',#4730);
#609=FACE_OUTER_BOUND('',#895,.T.);
#610=FACE_OUTER_BOUND('',#896,.T.);
#611=FACE_OUTER_BOUND('',#897,.T.);
#612=FACE_OUTER_BOUND('',#900,.T.);
#613=FACE_OUTER_BOUND('',#901,.T.);
#614=FACE_OUTER_BOUND('',#903,.T.);
#615=FACE_OUTER_BOUND('',#904,.T.);
#616=FACE_OUTER_BOUND('',#906,.T.);
#895=EDGE_LOOP('',(#3201,#3202,#3203,#3204));
#896=EDGE_LOOP('',(#3205,#3206,#3207,#3208));
#897=EDGE_LOOP('',(#3209,#3210));
#898=EDGE_LOOP('',(#3211));
#899=EDGE_LOOP('',(#3212));
#900=EDGE_LOOP('',(#3213,#3214,#3215,#3216));
#901=EDGE_LOOP('',(#3217));
#902=EDGE_LOOP('',(#3218));
#903=EDGE_LOOP('',(#3219,#3220,#3221,#3222));
#904=EDGE_LOOP('',(#3223));
#905=EDGE_LOOP('',(#3224));
#906=EDGE_LOOP('',(#3225));
#907=EDGE_LOOP('',(#3226));
#1228=LINE('',#6960,#1582);
#1229=LINE('',#6966,#1583);
#1230=LINE('',#6976,#1584);
#1231=LINE('',#6983,#1585);
#1582=VECTOR('',#5416,0.4);
#1583=VECTOR('',#5423,0.85);
#1584=VECTOR('',#5434,1.2);
#1585=VECTOR('',#5443,1.4);
#1892=CIRCLE('',#4715,0.4);
#1893=CIRCLE('',#4716,0.4);
#1894=CIRCLE('',#4718,0.85);
#1895=CIRCLE('',#4719,0.85);
#1896=CIRCLE('',#4721,1.);
#1897=CIRCLE('',#4723,1.2);
#1898=CIRCLE('',#4724,1.2);
#1899=CIRCLE('',#4727,1.4);
#1900=CIRCLE('',#4728,1.4);
#2110=VERTEX_POINT('',#6957);
#2111=VERTEX_POINT('',#6959);
#2112=VERTEX_POINT('',#6963);
#2113=VERTEX_POINT('',#6965);
#2114=VERTEX_POINT('',#6969);
#2115=VERTEX_POINT('',#6970);
#2116=VERTEX_POINT('',#6973);
#2117=VERTEX_POINT('',#6975);
#2118=VERTEX_POINT('',#6980);
#2119=VERTEX_POINT('',#6982);
#2518=EDGE_CURVE('',#2110,#2110,#1892,.T.);
#2519=EDGE_CURVE('',#2110,#2111,#1228,.T.);
#2520=EDGE_CURVE('',#2111,#2111,#1893,.T.);
#2521=EDGE_CURVE('',#2112,#2112,#1894,.T.);
#2522=EDGE_CURVE('',#2112,#2113,#1229,.T.);
#2523=EDGE_CURVE('',#2113,#2113,#1895,.T.);
#2524=EDGE_CURVE('',#2114,#2115,#1896,.T.);
#2525=EDGE_CURVE('',#2116,#2116,#1897,.T.);
#2526=EDGE_CURVE('',#2116,#2117,#1230,.T.);
#2527=EDGE_CURVE('',#2117,#2117,#1898,.T.);
#2528=EDGE_CURVE('',#2118,#2118,#1899,.T.);
#2529=EDGE_CURVE('',#2118,#2119,#1231,.T.);
#2530=EDGE_CURVE('',#2119,#2119,#1900,.T.);
#3201=ORIENTED_EDGE('',*,*,#2518,.F.);
#3202=ORIENTED_EDGE('',*,*,#2519,.T.);
#3203=ORIENTED_EDGE('',*,*,#2520,.F.);
#3204=ORIENTED_EDGE('',*,*,#2519,.F.);
#3205=ORIENTED_EDGE('',*,*,#2521,.F.);
#3206=ORIENTED_EDGE('',*,*,#2522,.T.);
#3207=ORIENTED_EDGE('',*,*,#2523,.F.);
#3208=ORIENTED_EDGE('',*,*,#2522,.F.);
#3209=ORIENTED_EDGE('',*,*,#2524,.T.);
#3210=ORIENTED_EDGE('',*,*,#2524,.F.);
#3211=ORIENTED_EDGE('',*,*,#2518,.T.);
#3212=ORIENTED_EDGE('',*,*,#2523,.T.);
#3213=ORIENTED_EDGE('',*,*,#2525,.F.);
#3214=ORIENTED_EDGE('',*,*,#2526,.T.);
#3215=ORIENTED_EDGE('',*,*,#2527,.F.);
#3216=ORIENTED_EDGE('',*,*,#2526,.F.);
#3217=ORIENTED_EDGE('',*,*,#2525,.T.);
#3218=ORIENTED_EDGE('',*,*,#2520,.T.);
#3219=ORIENTED_EDGE('',*,*,#2528,.F.);
#3220=ORIENTED_EDGE('',*,*,#2529,.T.);
#3221=ORIENTED_EDGE('',*,*,#2530,.T.);
#3222=ORIENTED_EDGE('',*,*,#2529,.F.);
#3223=ORIENTED_EDGE('',*,*,#2528,.T.);
#3224=ORIENTED_EDGE('',*,*,#2527,.T.);
#3225=ORIENTED_EDGE('',*,*,#2530,.F.);
#3226=ORIENTED_EDGE('',*,*,#2521,.T.);
#3980=CYLINDRICAL_SURFACE('',#4714,0.4);
#3981=CYLINDRICAL_SURFACE('',#4717,0.85);
#3982=CYLINDRICAL_SURFACE('',#4722,1.2);
#3983=CYLINDRICAL_SURFACE('',#4726,1.4);
#4099=ADVANCED_FACE('',(#609),#3980,.F.);
#4100=ADVANCED_FACE('',(#610),#3981,.F.);
#4101=ADVANCED_FACE('',(#611,#315,#316),#166,.F.);
#4102=ADVANCED_FACE('',(#612),#3982,.T.);
#4103=ADVANCED_FACE('',(#613,#317),#418,.T.);
#4104=ADVANCED_FACE('',(#614),#3983,.T.);
#4105=ADVANCED_FACE('',(#615,#318),#419,.T.);
#4106=ADVANCED_FACE('',(#616,#319),#420,.F.);
#4293=CLOSED_SHELL('',(#4099,#4100,#4101,#4102,#4103,#4104,#4105,#4106));
#4713=AXIS2_PLACEMENT_3D('',#6955,#5410,#5411);
#4714=AXIS2_PLACEMENT_3D('',#6956,#5412,#5413);
#4715=AXIS2_PLACEMENT_3D('',#6958,#5414,#5415);
#4716=AXIS2_PLACEMENT_3D('',#6961,#5417,#5418);
#4717=AXIS2_PLACEMENT_3D('',#6962,#5419,#5420);
#4718=AXIS2_PLACEMENT_3D('',#6964,#5421,#5422);
#4719=AXIS2_PLACEMENT_3D('',#6967,#5424,#5425);
#4720=AXIS2_PLACEMENT_3D('',#6968,#5426,#5427);
#4721=AXIS2_PLACEMENT_3D('',#6971,#5428,#5429);
#4722=AXIS2_PLACEMENT_3D('',#6972,#5430,#5431);
#4723=AXIS2_PLACEMENT_3D('',#6974,#5432,#5433);
#4724=AXIS2_PLACEMENT_3D('',#6977,#5435,#5436);
#4725=AXIS2_PLACEMENT_3D('',#6978,#5437,#5438);
#4726=AXIS2_PLACEMENT_3D('',#6979,#5439,#5440);
#4727=AXIS2_PLACEMENT_3D('',#6981,#5441,#5442);
#4728=AXIS2_PLACEMENT_3D('',#6984,#5444,#5445);
#4729=AXIS2_PLACEMENT_3D('',#6985,#5446,#5447);
#4730=AXIS2_PLACEMENT_3D('',#6986,#5448,#5449);
#5410=DIRECTION('axis',(0.,0.,1.));
#5411=DIRECTION('refdir',(1.,0.,0.));
#5412=DIRECTION('center_axis',(0.,1.,0.));
#5413=DIRECTION('ref_axis',(1.,0.,0.));
#5414=DIRECTION('center_axis',(0.,1.,0.));
#5415=DIRECTION('ref_axis',(1.,0.,0.));
#5416=DIRECTION('',(0.,1.,0.));
#5417=DIRECTION('center_axis',(0.,-1.,0.));
#5418=DIRECTION('ref_axis',(1.,0.,0.));
#5419=DIRECTION('center_axis',(0.,1.,0.));
#5420=DIRECTION('ref_axis',(1.,0.,0.));
#5421=DIRECTION('center_axis',(0.,1.,0.));
#5422=DIRECTION('ref_axis',(1.,0.,0.));
#5423=DIRECTION('',(0.,1.,0.));
#5424=DIRECTION('center_axis',(0.,-1.,0.));
#5425=DIRECTION('ref_axis',(1.,0.,0.));
#5426=DIRECTION('center_axis',(6.12323399573677E-17,0.,1.));
#5427=DIRECTION('ref_axis',(1.,0.,0.));
#5428=DIRECTION('center_axis',(0.,1.,0.));
#5429=DIRECTION('ref_axis',(-1.,0.,0.));
#5430=DIRECTION('center_axis',(0.,1.,0.));
#5431=DIRECTION('ref_axis',(1.,0.,0.));
#5432=DIRECTION('center_axis',(0.,1.,0.));
#5433=DIRECTION('ref_axis',(1.,0.,0.));
#5434=DIRECTION('',(0.,-1.,0.));
#5435=DIRECTION('center_axis',(0.,-1.,0.));
#5436=DIRECTION('ref_axis',(1.,0.,0.));
#5437=DIRECTION('center_axis',(0.,1.,0.));
#5438=DIRECTION('ref_axis',(1.,0.,0.));
#5439=DIRECTION('center_axis',(0.,1.,0.));
#5440=DIRECTION('ref_axis',(1.,0.,0.));
#5441=DIRECTION('center_axis',(0.,1.,0.));
#5442=DIRECTION('ref_axis',(1.,0.,0.));
#5443=DIRECTION('',(0.,-1.,0.));
#5444=DIRECTION('center_axis',(0.,1.,0.));
#5445=DIRECTION('ref_axis',(1.,0.,0.));
#5446=DIRECTION('center_axis',(0.,1.,0.));
#5447=DIRECTION('ref_axis',(1.,0.,0.));
#5448=DIRECTION('center_axis',(0.,1.,0.));
#5449=DIRECTION('ref_axis',(1.,0.,0.));
#6955=CARTESIAN_POINT('',(0.,0.,0.));
#6956=CARTESIAN_POINT('Origin',(0.,-2.1,23.));
#6957=CARTESIAN_POINT('',(-0.4,-1.08348486100883,23.));
#6958=CARTESIAN_POINT('Origin',(0.,-1.08348486100883,23.));
#6959=CARTESIAN_POINT('',(-0.4,-1.,23.));
#6960=CARTESIAN_POINT('',(-0.4,-2.1,23.));
#6961=CARTESIAN_POINT('Origin',(0.,-1.,23.));
#6962=CARTESIAN_POINT('Origin',(0.,-3.3,23.));
#6963=CARTESIAN_POINT('',(-0.85,-3.2,23.));
#6964=CARTESIAN_POINT('Origin',(0.,-3.2,23.));
#6965=CARTESIAN_POINT('',(-0.85,-2.52678268764264,23.));
#6966=CARTESIAN_POINT('',(-0.85,-3.3,23.));
#6967=CARTESIAN_POINT('Origin',(0.,-2.52678268764264,23.));
#6968=CARTESIAN_POINT('Origin',(0.,-2.,23.));
#6969=CARTESIAN_POINT('',(-6.12323399573677E-17,-2.,22.));
#6970=CARTESIAN_POINT('',(-6.12323399573677E-17,-2.,24.));
#6971=CARTESIAN_POINT('Origin',(0.,-2.,23.));
#6972=CARTESIAN_POINT('Origin',(0.,-1.5,23.));
#6973=CARTESIAN_POINT('',(-1.2,-1.,23.));
#6974=CARTESIAN_POINT('Origin',(0.,-1.,23.));
#6975=CARTESIAN_POINT('',(-1.2,-1.5,23.));
#6976=CARTESIAN_POINT('',(-1.2,-1.5,23.));
#6977=CARTESIAN_POINT('Origin',(0.,-1.5,23.));
#6978=CARTESIAN_POINT('Origin',(0.,-1.,23.));
#6979=CARTESIAN_POINT('Origin',(0.,-3.2,23.));
#6980=CARTESIAN_POINT('',(-1.4,-1.5,23.));
#6981=CARTESIAN_POINT('Origin',(0.,-1.5,23.));
#6982=CARTESIAN_POINT('',(-1.4,-3.2,23.));
#6983=CARTESIAN_POINT('',(-1.4,-3.2,23.));
#6984=CARTESIAN_POINT('Origin',(0.,-3.2,23.));
#6985=CARTESIAN_POINT('Origin',(0.,-1.5,23.));
#6986=CARTESIAN_POINT('Origin',(0.,-3.2,23.));
#7843=UNCERTAINTY_MEASURE_WITH_UNIT(LENGTH_MEASURE(0.001),#7898,
'DISTANCE_ACCURACY_VALUE',
'Maximum model space distance between geometric entities at asserted c
onnectivities');
#7865=UNCERTAINTY_MEASURE_WITH_UNIT(LENGTH_MEASURE(0.001),#7898,
'DISTANCE_ACCURACY_VALUE',
'Maximum model space distance between geometric entities at asserted c
onnectivities');
#7875=(
GEOMETRIC_REPRESENTATION_CONTEXT(3)
GLOBAL_UNCERTAINTY_ASSIGNED_CONTEXT((#7843))
GLOBAL_UNIT_ASSIGNED_CONTEXT((#7898,#7900,#7901))
REPRESENTATION_CONTEXT('','3D')
);
#7897=(
GEOMETRIC_REPRESENTATION_CONTEXT(3)
GLOBAL_UNCERTAINTY_ASSIGNED_CONTEXT((#7865))
GLOBAL_UNIT_ASSIGNED_CONTEXT((#7898,#7900,#7901))
REPRESENTATION_CONTEXT('','3D')
);
#7898=(
LENGTH_UNIT()
NAMED_UNIT(*)
SI_UNIT(.CENTI.,.METRE.)
);
#7900=(
NAMED_UNIT(*)
PLANE_ANGLE_UNIT()
SI_UNIT($,.RADIAN.)
);
#7901=(
NAMED_UNIT(*)
SI_UNIT($,.STERADIAN.)
SOLID_ANGLE_UNIT()
);
#7911=SHAPE_DEFINITION_REPRESENTATION(#7942,#8008);
#7942=PRODUCT_DEFINITION_SHAPE('',$,#8040);
#8008=SHAPE_REPRESENTATION('',(#4713),#7875);
#8030=PRODUCT_DEFINITION_CONTEXT('part definition',#8125,'design');
#8040=PRODUCT_DEFINITION('Ball clamp nut (1)','Ball clamp nut (1)',#8071,
#8030);
#8071=PRODUCT_DEFINITION_FORMATION('',$,#8136);
#8125=APPLICATION_CONTEXT(
'Core Data for Automotive Mechanical Design Process');
#8126=PRODUCT_CONTEXT('part definition',#8125,'mechanical');
#8136=PRODUCT('Ball clamp nut (1)','Ball clamp nut (1)','Ball clamp nut (1)',
(#8126));
#8221=COLOUR_RGB('Black',0.12,0.14,0.17);
#8222=FILL_AREA_STYLE_COLOUR('',#8221);
#8223=FILL_AREA_STYLE('',(#8222));
#8224=SURFACE_STYLE_FILL_AREA(#8223);
#8225=SURFACE_SIDE_STYLE('',(#8224));
#8226=SURFACE_STYLE_USAGE(.BOTH.,#8225);
#8227=PRESENTATION_STYLE_ASSIGNMENT((#8226));
ENDSEC;
END-ISO-10303-21;
